ISO-10303-21;
HEADER;
FILE_DESCRIPTION((''),'2;1');
FILE_NAME('Cover_Screw_1.step','2026-10-09T10:11:57-07:00',(''),(''),'','','');
FILE_SCHEMA (('AUTOMOTIVE_DESIGN { 1 0 10303 214 3 1 1 }'));
ENDSEC;
DATA;
#10=MECHANICAL_DESIGN_GEOMETRIC_PRESENTATION_REPRESENTATION('',(#129),#13510);
#99=SHAPE_REPRESENTATION_RELATIONSHIP('SRR','None',#13569,#114) ;
#114=ADVANCED_BREP_SHAPE_REPRESENTATION('',(#161),#13501) ;
#129=STYLED_ITEM('',(#13650),#161) ;
#161=MANIFOLD_SOLID_BREP('Body1',#7378) ;
#243=FACE_BOUND('',#1444,.T.) ;
#397=PLANE('',#8175) ;
#398=PLANE('',#8176) ;
#399=PLANE('',#8177) ;
#400=PLANE('',#8178) ;
#401=PLANE('',#8179) ;
#402=PLANE('',#8180) ;
#403=PLANE('',#8181) ;
#404=PLANE('',#8182) ;
#405=PLANE('',#8183) ;
#406=PLANE('',#8184) ;
#407=PLANE('',#8185) ;
#408=PLANE('',#8186) ;
#409=PLANE('',#8187) ;
#410=PLANE('',#8188) ;
#411=PLANE('',#8189) ;
#412=PLANE('',#8190) ;
#413=PLANE('',#8191) ;
#414=PLANE('',#8192) ;
#415=PLANE('',#8193) ;
#638=CYLINDRICAL_SURFACE('',#8166,2.6) ;
#639=CYLINDRICAL_SURFACE('',#8171,1.5) ;
#926=FACE_OUTER_BOUND('',#1430,.T.) ;
#927=FACE_OUTER_BOUND('',#1431,.T.) ;
#928=FACE_OUTER_BOUND('',#1432,.T.) ;
#929=FACE_OUTER_BOUND('',#1433,.T.) ;
#930=FACE_OUTER_BOUND('',#1434,.T.) ;
#931=FACE_OUTER_BOUND('',#1435,.T.) ;
#932=FACE_OUTER_BOUND('',#1436,.T.) ;
#933=FACE_OUTER_BOUND('',#1437,.T.) ;
#934=FACE_OUTER_BOUND('',#1438,.T.) ;
#935=FACE_OUTER_BOUND('',#1439,.T.) ;
#936=FACE_OUTER_BOUND('',#1440,.T.) ;
#937=FACE_OUTER_BOUND('',#1441,.T.) ;
#938=FACE_OUTER_BOUND('',#1442,.T.) ;
#939=FACE_OUTER_BOUND('',#1443,.T.) ;
#940=FACE_OUTER_BOUND('',#1445,.T.) ;
#941=FACE_OUTER_BOUND('',#1446,.T.) ;
#942=FACE_OUTER_BOUND('',#1447,.T.) ;
#943=FACE_OUTER_BOUND('',#1448,.T.) ;
#944=FACE_OUTER_BOUND('',#1449,.T.) ;
#945=FACE_OUTER_BOUND('',#1450,.T.) ;
#946=FACE_OUTER_BOUND('',#1451,.T.) ;
#947=FACE_OUTER_BOUND('',#1452,.T.) ;
#948=FACE_OUTER_BOUND('',#1453,.T.) ;
#1430=EDGE_LOOP('',(#6146,#6147,#6148,#6149)) ;
#1431=EDGE_LOOP('',(#6150,#6151,#6152,#6153)) ;
#1432=EDGE_LOOP('',(#6154,#6155,#6156,#6157)) ;
#1433=EDGE_LOOP('',(#6158,#6159,#6160,#6161)) ;
#1434=EDGE_LOOP('',(#6162)) ;
#1435=EDGE_LOOP('',(#6163,#6164,#6165,#6166)) ;
#1436=EDGE_LOOP('',(#6167,#6168,#6169,#6170)) ;
#1437=EDGE_LOOP('',(#6171,#6172,#6173,#6174)) ;
#1438=EDGE_LOOP('',(#6175,#6176,#6177,#6178)) ;
#1439=EDGE_LOOP('',(#6179,#6180,#6181,#6182)) ;
#1440=EDGE_LOOP('',(#6183,#6184,#6185,#6186)) ;
#1441=EDGE_LOOP('',(#6187,#6188,#6189,#6190)) ;
#1442=EDGE_LOOP('',(#6191,#6192,#6193,#6194)) ;
#1443=EDGE_LOOP('',(#6195)) ;
#1444=EDGE_LOOP('',(#6196,#6197,#6198,#6199,#6200,#6201,#6202,#6203,#6204,
#6205,#6206,#6207)) ;
#1445=EDGE_LOOP('',(#6208,#6209,#6210,#6211)) ;
#1446=EDGE_LOOP('',(#6212,#6213,#6214,#6215)) ;
#1447=EDGE_LOOP('',(#6216,#6217,#6218,#6219)) ;
#1448=EDGE_LOOP('',(#6220,#6221,#6222,#6223)) ;
#1449=EDGE_LOOP('',(#6224,#6225,#6226,#6227)) ;
#1450=EDGE_LOOP('',(#6228,#6229,#6230,#6231)) ;
#1451=EDGE_LOOP('',(#6232,#6233,#6234,#6235)) ;
#1452=EDGE_LOOP('',(#6236,#6237,#6238,#6239)) ;
#1453=EDGE_LOOP('',(#6240,#6241,#6242,#6243)) ;
#1963=LINE('',#12667,#2457) ;
#1964=LINE('',#12671,#2458) ;
#1965=LINE('',#12675,#2459) ;
#1966=LINE('',#12679,#2460) ;
#1967=LINE('',#12685,#2461) ;
#1968=LINE('',#12687,#2462) ;
#1969=LINE('',#12689,#2463) ;
#1970=LINE('',#12690,#2464) ;
#1971=LINE('',#12694,#2465) ;
#1972=LINE('',#12696,#2466) ;
#1973=LINE('',#12698,#2467) ;
#1974=LINE('',#12699,#2468) ;
#1975=LINE('',#12702,#2469) ;
#1976=LINE('',#12704,#2470) ;
#1977=LINE('',#12705,#2471) ;
#1978=LINE('',#12709,#2472) ;
#1979=LINE('',#12710,#2473) ;
#1980=LINE('',#12711,#2474) ;
#1981=LINE('',#12714,#2475) ;
#1982=LINE('',#12715,#2476) ;
#1983=LINE('',#12718,#2477) ;
#1984=LINE('',#12719,#2478) ;
#1985=LINE('',#12722,#2479) ;
#1986=LINE('',#12723,#2480) ;
#1987=LINE('',#12726,#2481) ;
#1988=LINE('',#12727,#2482) ;
#1989=LINE('',#12730,#2483) ;
#1990=LINE('',#12732,#2484) ;
#1991=LINE('',#12733,#2485) ;
#1992=LINE('',#12735,#2486) ;
#1993=LINE('',#12737,#2487) ;
#1994=LINE('',#12738,#2488) ;
#1995=LINE('',#12742,#2489) ;
#1996=LINE('',#12743,#2490) ;
#1997=LINE('',#12744,#2491) ;
#1998=LINE('',#12745,#2492) ;
#1999=LINE('',#12747,#2493) ;
#2000=LINE('',#12748,#2494) ;
#2001=LINE('',#12752,#2495) ;
#2002=LINE('',#12754,#2496) ;
#2003=LINE('',#12756,#2497) ;
#2004=LINE('',#12757,#2498) ;
#2005=LINE('',#12759,#2499) ;
#2006=LINE('',#12761,#2500) ;
#2457=VECTOR('',#10077,2.6) ;
#2458=VECTOR('',#10082,1.5) ;
#2459=VECTOR('',#10087,1.5) ;
#2460=VECTOR('',#10092,1.2) ;
#2461=VECTOR('',#10099,1.) ;
#2462=VECTOR('',#10100,1.00000000000064) ;
#2463=VECTOR('',#10101,1.) ;
#2464=VECTOR('',#10102,1.00000000000064) ;
#2465=VECTOR('',#10105,1.) ;
#2466=VECTOR('',#10106,1.00000000000064) ;
#2467=VECTOR('',#10107,1.) ;
#2468=VECTOR('',#10108,1.00000000000064) ;
#2469=VECTOR('',#10111,1.) ;
#2470=VECTOR('',#10112,1.) ;
#2471=VECTOR('',#10113,1.) ;
#2472=VECTOR('',#10116,1.) ;
#2473=VECTOR('',#10117,1.) ;
#2474=VECTOR('',#10118,1.) ;
#2475=VECTOR('',#10121,1.) ;
#2476=VECTOR('',#10122,1.) ;
#2477=VECTOR('',#10125,1.) ;
#2478=VECTOR('',#10126,1.) ;
#2479=VECTOR('',#10129,1.) ;
#2480=VECTOR('',#10130,1.) ;
#2481=VECTOR('',#10133,1.) ;
#2482=VECTOR('',#10134,1.) ;
#2483=VECTOR('',#10137,1.) ;
#2484=VECTOR('',#10138,1.) ;
#2485=VECTOR('',#10139,1.) ;
#2486=VECTOR('',#10140,1.) ;
#2487=VECTOR('',#10141,1.) ;
#2488=VECTOR('',#10142,1.) ;
#2489=VECTOR('',#10145,1.) ;
#2490=VECTOR('',#10146,1.00000000000064) ;
#2491=VECTOR('',#10147,1.) ;
#2492=VECTOR('',#10148,1.00000000000064) ;
#2493=VECTOR('',#10151,1.) ;
#2494=VECTOR('',#10152,1.) ;
#2495=VECTOR('',#10159,1.) ;
#2496=VECTOR('',#10160,1.00000000000064) ;
#2497=VECTOR('',#10161,1.) ;
#2498=VECTOR('',#10162,1.00000000000064) ;
#2499=VECTOR('',#10165,1.) ;
#2500=VECTOR('',#10168,1.) ;
#2961=CIRCLE('',#8167,2.6) ;
#2962=CIRCLE('',#8168,2.6) ;
#2963=CIRCLE('',#8170,1.5) ;
#2964=CIRCLE('',#8172,1.5) ;
#2965=CIRCLE('',#8174,1.2) ;
#3565=VERTEX_POINT('',#12664) ;
#3566=VERTEX_POINT('',#12666) ;
#3567=VERTEX_POINT('',#12670) ;
#3568=VERTEX_POINT('',#12674) ;
#3569=VERTEX_POINT('',#12678) ;
#3570=VERTEX_POINT('',#12683) ;
#3571=VERTEX_POINT('',#12684) ;
#3572=VERTEX_POINT('',#12686) ;
#3573=VERTEX_POINT('',#12688) ;
#3574=VERTEX_POINT('',#12692) ;
#3575=VERTEX_POINT('',#12693) ;
#3576=VERTEX_POINT('',#12695) ;
#3577=VERTEX_POINT('',#12697) ;
#3578=VERTEX_POINT('',#12701) ;
#3579=VERTEX_POINT('',#12703) ;
#3580=VERTEX_POINT('',#12707) ;
#3581=VERTEX_POINT('',#12708) ;
#3582=VERTEX_POINT('',#12713) ;
#3583=VERTEX_POINT('',#12717) ;
#3584=VERTEX_POINT('',#12721) ;
#3585=VERTEX_POINT('',#12725) ;
#3586=VERTEX_POINT('',#12729) ;
#3587=VERTEX_POINT('',#12731) ;
#3588=VERTEX_POINT('',#12734) ;
#3589=VERTEX_POINT('',#12736) ;
#3590=VERTEX_POINT('',#12740) ;
#3591=VERTEX_POINT('',#12741) ;
#3592=VERTEX_POINT('',#12753) ;
#3593=VERTEX_POINT('',#12755) ;
#4460=EDGE_CURVE('',#3565,#3565,#2961,.T.) ;
#4461=EDGE_CURVE('',#3565,#3566,#1963,.T.) ;
#4462=EDGE_CURVE('',#3566,#3566,#2962,.T.) ;
#4463=EDGE_CURVE('',#3566,#3567,#1964,.T.) ;
#4464=EDGE_CURVE('',#3567,#3567,#2963,.T.) ;
#4465=EDGE_CURVE('',#3567,#3568,#1965,.T.) ;
#4466=EDGE_CURVE('',#3568,#3568,#2964,.T.) ;
#4467=EDGE_CURVE('',#3568,#3569,#1966,.T.) ;
#4468=EDGE_CURVE('',#3569,#3569,#2965,.T.) ;
#4469=EDGE_CURVE('',#3570,#3571,#1967,.T.) ;
#4470=EDGE_CURVE('',#3570,#3572,#1968,.T.) ;
#4471=EDGE_CURVE('',#3572,#3573,#1969,.T.) ;
#4472=EDGE_CURVE('',#3571,#3573,#1970,.T.) ;
#4473=EDGE_CURVE('',#3574,#3575,#1971,.T.) ;
#4474=EDGE_CURVE('',#3574,#3576,#1972,.F.) ;
#4475=EDGE_CURVE('',#3576,#3577,#1973,.T.) ;
#4476=EDGE_CURVE('',#3575,#3577,#1974,.F.) ;
#4477=EDGE_CURVE('',#3572,#3578,#1975,.T.) ;
#4478=EDGE_CURVE('',#3578,#3579,#1976,.T.) ;
#4479=EDGE_CURVE('',#3573,#3579,#1977,.T.) ;
#4480=EDGE_CURVE('',#3580,#3581,#1978,.T.) ;
#4481=EDGE_CURVE('',#3580,#3574,#1979,.F.) ;
#4482=EDGE_CURVE('',#3581,#3575,#1980,.F.) ;
#4483=EDGE_CURVE('',#3579,#3582,#1981,.T.) ;
#4484=EDGE_CURVE('',#3582,#3571,#1982,.T.) ;
#4485=EDGE_CURVE('',#3583,#3581,#1983,.F.) ;
#4486=EDGE_CURVE('',#3583,#3577,#1984,.T.) ;
#4487=EDGE_CURVE('',#3584,#3570,#1985,.T.) ;
#4488=EDGE_CURVE('',#3578,#3584,#1986,.T.) ;
#4489=EDGE_CURVE('',#3585,#3576,#1987,.T.) ;
#4490=EDGE_CURVE('',#3585,#3580,#1988,.F.) ;
#4491=EDGE_CURVE('',#3584,#3586,#1989,.F.) ;
#4492=EDGE_CURVE('',#3586,#3587,#1990,.T.) ;
#4493=EDGE_CURVE('',#3585,#3587,#1991,.F.) ;
#4494=EDGE_CURVE('',#3588,#3583,#1992,.T.) ;
#4495=EDGE_CURVE('',#3589,#3588,#1993,.T.) ;
#4496=EDGE_CURVE('',#3589,#3582,#1994,.T.) ;
#4497=EDGE_CURVE('',#3590,#3591,#1995,.T.) ;
#4498=EDGE_CURVE('',#3590,#3570,#1996,.F.) ;
#4499=EDGE_CURVE('',#3570,#3576,#1997,.T.) ;
#4500=EDGE_CURVE('',#3591,#3576,#1998,.F.) ;
#4501=EDGE_CURVE('',#3586,#3590,#1999,.F.) ;
#4502=EDGE_CURVE('',#3587,#3591,#2000,.F.) ;
#4503=EDGE_CURVE('',#3571,#3577,#2001,.T.) ;
#4504=EDGE_CURVE('',#3571,#3592,#2002,.T.) ;
#4505=EDGE_CURVE('',#3592,#3593,#2003,.T.) ;
#4506=EDGE_CURVE('',#3577,#3593,#2004,.T.) ;
#4507=EDGE_CURVE('',#3592,#3589,#2005,.T.) ;
#4508=EDGE_CURVE('',#3593,#3588,#2006,.T.) ;
#6146=ORIENTED_EDGE('',*,*,#4460,.F.) ;
#6147=ORIENTED_EDGE('',*,*,#4461,.T.) ;
#6148=ORIENTED_EDGE('',*,*,#4462,.T.) ;
#6149=ORIENTED_EDGE('',*,*,#4461,.F.) ;
#6150=ORIENTED_EDGE('',*,*,#4462,.F.) ;
#6151=ORIENTED_EDGE('',*,*,#4463,.T.) ;
#6152=ORIENTED_EDGE('',*,*,#4464,.T.) ;
#6153=ORIENTED_EDGE('',*,*,#4463,.F.) ;
#6154=ORIENTED_EDGE('',*,*,#4464,.F.) ;
#6155=ORIENTED_EDGE('',*,*,#4465,.T.) ;
#6156=ORIENTED_EDGE('',*,*,#4466,.T.) ;
#6157=ORIENTED_EDGE('',*,*,#4465,.F.) ;
#6158=ORIENTED_EDGE('',*,*,#4466,.F.) ;
#6159=ORIENTED_EDGE('',*,*,#4467,.T.) ;
#6160=ORIENTED_EDGE('',*,*,#4468,.T.) ;
#6161=ORIENTED_EDGE('',*,*,#4467,.F.) ;
#6162=ORIENTED_EDGE('',*,*,#4468,.F.) ;
#6163=ORIENTED_EDGE('',*,*,#4469,.F.) ;
#6164=ORIENTED_EDGE('',*,*,#4470,.T.) ;
#6165=ORIENTED_EDGE('',*,*,#4471,.T.) ;
#6166=ORIENTED_EDGE('',*,*,#4472,.F.) ;
#6167=ORIENTED_EDGE('',*,*,#4473,.F.) ;
#6168=ORIENTED_EDGE('',*,*,#4474,.T.) ;
#6169=ORIENTED_EDGE('',*,*,#4475,.T.) ;
#6170=ORIENTED_EDGE('',*,*,#4476,.F.) ;
#6171=ORIENTED_EDGE('',*,*,#4471,.F.) ;
#6172=ORIENTED_EDGE('',*,*,#4477,.T.) ;
#6173=ORIENTED_EDGE('',*,*,#4478,.T.) ;
#6174=ORIENTED_EDGE('',*,*,#4479,.F.) ;
#6175=ORIENTED_EDGE('',*,*,#4480,.F.) ;
#6176=ORIENTED_EDGE('',*,*,#4481,.T.) ;
#6177=ORIENTED_EDGE('',*,*,#4473,.T.) ;
#6178=ORIENTED_EDGE('',*,*,#4482,.F.) ;
#6179=ORIENTED_EDGE('',*,*,#4472,.T.) ;
#6180=ORIENTED_EDGE('',*,*,#4479,.T.) ;
#6181=ORIENTED_EDGE('',*,*,#4483,.T.) ;
#6182=ORIENTED_EDGE('',*,*,#4484,.T.) ;
#6183=ORIENTED_EDGE('',*,*,#4485,.T.) ;
#6184=ORIENTED_EDGE('',*,*,#4482,.T.) ;
#6185=ORIENTED_EDGE('',*,*,#4476,.T.) ;
#6186=ORIENTED_EDGE('',*,*,#4486,.F.) ;
#6187=ORIENTED_EDGE('',*,*,#4487,.F.) ;
#6188=ORIENTED_EDGE('',*,*,#4488,.F.) ;
#6189=ORIENTED_EDGE('',*,*,#4477,.F.) ;
#6190=ORIENTED_EDGE('',*,*,#4470,.F.) ;
#6191=ORIENTED_EDGE('',*,*,#4489,.T.) ;
#6192=ORIENTED_EDGE('',*,*,#4474,.F.) ;
#6193=ORIENTED_EDGE('',*,*,#4481,.F.) ;
#6194=ORIENTED_EDGE('',*,*,#4490,.F.) ;
#6195=ORIENTED_EDGE('',*,*,#4460,.T.) ;
#6196=ORIENTED_EDGE('',*,*,#4483,.F.) ;
#6197=ORIENTED_EDGE('',*,*,#4478,.F.) ;
#6198=ORIENTED_EDGE('',*,*,#4488,.T.) ;
#6199=ORIENTED_EDGE('',*,*,#4491,.T.) ;
#6200=ORIENTED_EDGE('',*,*,#4492,.T.) ;
#6201=ORIENTED_EDGE('',*,*,#4493,.F.) ;
#6202=ORIENTED_EDGE('',*,*,#4490,.T.) ;
#6203=ORIENTED_EDGE('',*,*,#4480,.T.) ;
#6204=ORIENTED_EDGE('',*,*,#4485,.F.) ;
#6205=ORIENTED_EDGE('',*,*,#4494,.F.) ;
#6206=ORIENTED_EDGE('',*,*,#4495,.F.) ;
#6207=ORIENTED_EDGE('',*,*,#4496,.T.) ;
#6208=ORIENTED_EDGE('',*,*,#4497,.F.) ;
#6209=ORIENTED_EDGE('',*,*,#4498,.T.) ;
#6210=ORIENTED_EDGE('',*,*,#4499,.T.) ;
#6211=ORIENTED_EDGE('',*,*,#4500,.F.) ;
#6212=ORIENTED_EDGE('',*,*,#4492,.F.) ;
#6213=ORIENTED_EDGE('',*,*,#4501,.T.) ;
#6214=ORIENTED_EDGE('',*,*,#4497,.T.) ;
#6215=ORIENTED_EDGE('',*,*,#4502,.F.) ;
#6216=ORIENTED_EDGE('',*,*,#4487,.T.) ;
#6217=ORIENTED_EDGE('',*,*,#4498,.F.) ;
#6218=ORIENTED_EDGE('',*,*,#4501,.F.) ;
#6219=ORIENTED_EDGE('',*,*,#4491,.F.) ;
#6220=ORIENTED_EDGE('',*,*,#4493,.T.) ;
#6221=ORIENTED_EDGE('',*,*,#4502,.T.) ;
#6222=ORIENTED_EDGE('',*,*,#4500,.T.) ;
#6223=ORIENTED_EDGE('',*,*,#4489,.F.) ;
#6224=ORIENTED_EDGE('',*,*,#4503,.F.) ;
#6225=ORIENTED_EDGE('',*,*,#4504,.T.) ;
#6226=ORIENTED_EDGE('',*,*,#4505,.T.) ;
#6227=ORIENTED_EDGE('',*,*,#4506,.F.) ;
#6228=ORIENTED_EDGE('',*,*,#4484,.F.) ;
#6229=ORIENTED_EDGE('',*,*,#4496,.F.) ;
#6230=ORIENTED_EDGE('',*,*,#4507,.F.) ;
#6231=ORIENTED_EDGE('',*,*,#4504,.F.) ;
#6232=ORIENTED_EDGE('',*,*,#4505,.F.) ;
#6233=ORIENTED_EDGE('',*,*,#4507,.T.) ;
#6234=ORIENTED_EDGE('',*,*,#4495,.T.) ;
#6235=ORIENTED_EDGE('',*,*,#4508,.F.) ;
#6236=ORIENTED_EDGE('',*,*,#4506,.T.) ;
#6237=ORIENTED_EDGE('',*,*,#4508,.T.) ;
#6238=ORIENTED_EDGE('',*,*,#4494,.T.) ;
#6239=ORIENTED_EDGE('',*,*,#4486,.T.) ;
#6240=ORIENTED_EDGE('',*,*,#4499,.F.) ;
#6241=ORIENTED_EDGE('',*,*,#4469,.T.) ;
#6242=ORIENTED_EDGE('',*,*,#4503,.T.) ;
#6243=ORIENTED_EDGE('',*,*,#4475,.F.) ;
#6888=CONICAL_SURFACE('',#8169,1.5,0.785398163397) ;
#6889=CONICAL_SURFACE('',#8173,1.2,0.785398163397) ;
#7176=ADVANCED_FACE('',(#926),#638,.T.) ;
#7177=ADVANCED_FACE('',(#927),#6888,.T.) ;
#7178=ADVANCED_FACE('',(#928),#639,.T.) ;
#7179=ADVANCED_FACE('',(#929),#6889,.T.) ;
#7180=ADVANCED_FACE('',(#930),#397,.F.) ;
#7181=ADVANCED_FACE('',(#931),#398,.T.) ;
#7182=ADVANCED_FACE('',(#932),#399,.F.) ;
#7183=ADVANCED_FACE('',(#933),#400,.T.) ;
#7184=ADVANCED_FACE('',(#934),#401,.F.) ;
#7185=ADVANCED_FACE('',(#935),#402,.T.) ;
#7186=ADVANCED_FACE('',(#936),#403,.T.) ;
#7187=ADVANCED_FACE('',(#937),#404,.F.) ;
#7188=ADVANCED_FACE('',(#938),#405,.F.) ;
#7189=ADVANCED_FACE('',(#939,#243),#406,.T.) ;
#7190=ADVANCED_FACE('',(#940),#407,.F.) ;
#7191=ADVANCED_FACE('',(#941),#408,.F.) ;
#7192=ADVANCED_FACE('',(#942),#409,.F.) ;
#7193=ADVANCED_FACE('',(#943),#410,.T.) ;
#7194=ADVANCED_FACE('',(#944),#411,.T.) ;
#7195=ADVANCED_FACE('',(#945),#412,.F.) ;
#7196=ADVANCED_FACE('',(#946),#413,.T.) ;
#7197=ADVANCED_FACE('',(#947),#414,.T.) ;
#7198=ADVANCED_FACE('',(#948),#415,.T.) ;
#7378=CLOSED_SHELL('',(#7176,#7177,#7178,#7179,#7180,#7181,#7182,#7183,
#7184,#7185,#7186,#7187,#7188,#7189,#7190,#7191,#7192,#7193,#7194,#7195,
#7196,#7197,#7198)) ;
#8165=AXIS2_PLACEMENT_3D('',#12662,#10071,#10072) ;
#8166=AXIS2_PLACEMENT_3D('',#12663,#10073,#10074) ;
#8167=AXIS2_PLACEMENT_3D('',#12665,#10075,#10076) ;
#8168=AXIS2_PLACEMENT_3D('',#12668,#10078,#10079) ;
#8169=AXIS2_PLACEMENT_3D('',#12669,#10080,#10081) ;
#8170=AXIS2_PLACEMENT_3D('',#12672,#10083,#10084) ;
#8171=AXIS2_PLACEMENT_3D('',#12673,#10085,#10086) ;
#8172=AXIS2_PLACEMENT_3D('',#12676,#10088,#10089) ;
#8173=AXIS2_PLACEMENT_3D('',#12677,#10090,#10091) ;
#8174=AXIS2_PLACEMENT_3D('',#12680,#10093,#10094) ;
#8175=AXIS2_PLACEMENT_3D('',#12681,#10095,#10096) ;
#8176=AXIS2_PLACEMENT_3D('',#12682,#10097,#10098) ;
#8177=AXIS2_PLACEMENT_3D('',#12691,#10103,#10104) ;
#8178=AXIS2_PLACEMENT_3D('',#12700,#10109,#10110) ;
#8179=AXIS2_PLACEMENT_3D('',#12706,#10114,#10115) ;
#8180=AXIS2_PLACEMENT_3D('',#12712,#10119,#10120) ;
#8181=AXIS2_PLACEMENT_3D('',#12716,#10123,#10124) ;
#8182=AXIS2_PLACEMENT_3D('',#12720,#10127,#10128) ;
#8183=AXIS2_PLACEMENT_3D('',#12724,#10131,#10132) ;
#8184=AXIS2_PLACEMENT_3D('',#12728,#10135,#10136) ;
#8185=AXIS2_PLACEMENT_3D('',#12739,#10143,#10144) ;
#8186=AXIS2_PLACEMENT_3D('',#12746,#10149,#10150) ;
#8187=AXIS2_PLACEMENT_3D('',#12749,#10153,#10154) ;
#8188=AXIS2_PLACEMENT_3D('',#12750,#10155,#10156) ;
#8189=AXIS2_PLACEMENT_3D('',#12751,#10157,#10158) ;
#8190=AXIS2_PLACEMENT_3D('',#12758,#10163,#10164) ;
#8191=AXIS2_PLACEMENT_3D('',#12760,#10166,#10167) ;
#8192=AXIS2_PLACEMENT_3D('',#12762,#10169,#10170) ;
#8193=AXIS2_PLACEMENT_3D('',#12763,#10171,#10172) ;
#10071=DIRECTION('axis',(0.,0.,1.)) ;
#10072=DIRECTION('refdir',(1.,0.,0.)) ;
#10073=DIRECTION('center_axis',(0.,0.,1.)) ;
#10074=DIRECTION('ref_axis',(0.479425538604204,-0.877582561890372,0.)) ;
#10075=DIRECTION('center_axis',(0.,0.,1.)) ;
#10076=DIRECTION('ref_axis',(-1.,0.,0.)) ;
#10077=DIRECTION('',(0.,0.,-1.)) ;
#10078=DIRECTION('center_axis',(0.,0.,1.)) ;
#10079=DIRECTION('ref_axis',(-1.,0.,0.)) ;
#10080=DIRECTION('center_axis',(0.,0.,1.)) ;
#10081=DIRECTION('ref_axis',(0.479425538604204,-0.877582561890372,0.)) ;
#10082=DIRECTION('',(0.339005049420894,-0.620544580563467,-0.707106781186865)) ;
#10083=DIRECTION('center_axis',(0.,0.,1.)) ;
#10084=DIRECTION('ref_axis',(-1.,0.,0.)) ;
#10085=DIRECTION('center_axis',(0.,0.,1.)) ;
#10086=DIRECTION('ref_axis',(0.479425538604204,-0.877582561890372,0.)) ;
#10087=DIRECTION('',(0.,0.,-1.)) ;
#10088=DIRECTION('center_axis',(0.,0.,1.)) ;
#10089=DIRECTION('ref_axis',(-1.,0.,0.)) ;
#10090=DIRECTION('center_axis',(0.,0.,1.)) ;
#10091=DIRECTION('ref_axis',(0.479425538604203,-0.877582561890373,0.)) ;
#10092=DIRECTION('',(0.339005049420893,-0.620544580563467,-0.707106781186865)) ;
#10093=DIRECTION('center_axis',(0.,0.,1.)) ;
#10094=DIRECTION('ref_axis',(-1.,0.,0.)) ;
#10095=DIRECTION('center_axis',(0.,0.,1.)) ;
#10096=DIRECTION('ref_axis',(1.,0.,0.)) ;
#10097=DIRECTION('center_axis',(0.,-0.707106781186548,0.707106781186548)) ;
#10098=DIRECTION('ref_axis',(0.,0.707106781186548,0.707106781186548)) ;
#10099=DIRECTION('',(-1.,0.,0.)) ;
#10100=DIRECTION('',(0.,0.707106781186548,0.707106781186548)) ;
#10101=DIRECTION('',(-1.,0.,0.)) ;
#10102=DIRECTION('',(0.,0.707106781186548,0.707106781186548)) ;
#10103=DIRECTION('center_axis',(0.,-0.707106781186548,-0.707106781186548)) ;
#10104=DIRECTION('ref_axis',(0.,-0.707106781186548,0.707106781186548)) ;
#10105=DIRECTION('',(-1.,0.,0.)) ;
#10106=DIRECTION('',(0.,-0.707106781186548,0.707106781186548)) ;
#10107=DIRECTION('',(-1.,0.,0.)) ;
#10108=DIRECTION('',(0.,-0.707106781186548,0.707106781186548)) ;
#10109=DIRECTION('center_axis',(0.,-1.,0.)) ;
#10110=DIRECTION('ref_axis',(0.,0.,1.)) ;
#10111=DIRECTION('',(0.,0.,1.)) ;
#10112=DIRECTION('',(-1.,0.,0.)) ;
#10113=DIRECTION('',(0.,0.,1.)) ;
#10114=DIRECTION('center_axis',(0.,-1.,0.)) ;
#10115=DIRECTION('ref_axis',(0.,0.,1.)) ;
#10116=DIRECTION('',(-1.,0.,0.)) ;
#10117=DIRECTION('',(0.,0.,1.)) ;
#10118=DIRECTION('',(0.,0.,1.)) ;
#10119=DIRECTION('center_axis',(1.,0.,0.)) ;
#10120=DIRECTION('ref_axis',(0.,1.,0.)) ;
#10121=DIRECTION('',(0.,-1.,0.)) ;
#10122=DIRECTION('',(0.,0.,-1.)) ;
#10123=DIRECTION('center_axis',(1.,0.,0.)) ;
#10124=DIRECTION('ref_axis',(0.,1.,0.)) ;
#10125=DIRECTION('',(0.,1.,0.)) ;
#10126=DIRECTION('',(0.,0.,-1.)) ;
#10127=DIRECTION('center_axis',(1.,0.,0.)) ;
#10128=DIRECTION('ref_axis',(0.,1.,0.)) ;
#10129=DIRECTION('',(0.,0.,-1.)) ;
#10130=DIRECTION('',(0.,-1.,0.)) ;
#10131=DIRECTION('center_axis',(1.,0.,0.)) ;
#10132=DIRECTION('ref_axis',(0.,1.,0.)) ;
#10133=DIRECTION('',(0.,0.,-1.)) ;
#10134=DIRECTION('',(0.,1.,0.)) ;
#10135=DIRECTION('center_axis',(0.,0.,1.)) ;
#10136=DIRECTION('ref_axis',(1.,0.,0.)) ;
#10137=DIRECTION('',(-1.,0.,0.)) ;
#10138=DIRECTION('',(0.,-1.,0.)) ;
#10139=DIRECTION('',(-1.,0.,0.)) ;
#10140=DIRECTION('',(1.,0.,0.)) ;
#10141=DIRECTION('',(0.,-1.,0.)) ;
#10142=DIRECTION('',(1.,0.,0.)) ;
#10143=DIRECTION('center_axis',(0.707106781186548,-4.32978028117723E-17,
-0.707106781186548)) ;
#10144=DIRECTION('ref_axis',(0.707106781186548,-4.32978028117723E-17,0.707106781186548)) ;
#10145=DIRECTION('',(0.,-1.,0.)) ;
#10146=DIRECTION('',(0.707106781186548,0.,0.707106781186548)) ;
#10147=DIRECTION('',(0.,-1.,0.)) ;
#10148=DIRECTION('',(0.707106781186548,0.,0.707106781186548)) ;
#10149=DIRECTION('center_axis',(1.,-6.12323399574E-17,0.)) ;
#10150=DIRECTION('ref_axis',(0.,0.,1.)) ;
#10151=DIRECTION('',(0.,0.,1.)) ;
#10152=DIRECTION('',(0.,0.,1.)) ;
#10153=DIRECTION('center_axis',(6.12323399574E-17,1.,0.)) ;
#10154=DIRECTION('ref_axis',(-1.,6.12323399574E-17,0.)) ;
#10155=DIRECTION('center_axis',(6.12323399574E-17,1.,0.)) ;
#10156=DIRECTION('ref_axis',(-1.,6.12323399574E-17,0.)) ;
#10157=DIRECTION('center_axis',(0.707106781186548,-4.32978028117723E-17,
0.707106781186548)) ;
#10158=DIRECTION('ref_axis',(-0.707106781186548,4.32978028117723E-17,0.707106781186548)) ;
#10159=DIRECTION('',(0.,-1.,0.)) ;
#10160=DIRECTION('',(-0.707106781186548,0.,0.707106781186548)) ;
#10161=DIRECTION('',(0.,-1.,0.)) ;
#10162=DIRECTION('',(-0.707106781186548,0.,0.707106781186548)) ;
#10163=DIRECTION('center_axis',(6.12323399574E-17,1.,0.)) ;
#10164=DIRECTION('ref_axis',(-1.,6.12323399574E-17,0.)) ;
#10165=DIRECTION('',(0.,0.,1.)) ;
#10166=DIRECTION('center_axis',(1.,-6.12323399574E-17,0.)) ;
#10167=DIRECTION('ref_axis',(0.,0.,1.)) ;
#10168=DIRECTION('',(0.,0.,1.)) ;
#10169=DIRECTION('center_axis',(6.12323399574E-17,1.,0.)) ;
#10170=DIRECTION('ref_axis',(-1.,6.12323399574E-17,0.)) ;
#10171=DIRECTION('center_axis',(0.,0.,1.)) ;
#10172=DIRECTION('ref_axis',(0.,1.,0.)) ;
#12662=CARTESIAN_POINT('',(0.,0.,0.)) ;
#12663=CARTESIAN_POINT('Origin',(0.,-25.,128.75)) ;
#12664=CARTESIAN_POINT('',(-1.24650640037,-22.7182853391,143.75)) ;
#12665=CARTESIAN_POINT('Origin',(0.,-25.,143.75)) ;
#12666=CARTESIAN_POINT('',(-1.24650640037,-22.7182853391,143.25)) ;
#12667=CARTESIAN_POINT('',(-1.24650640037093,-22.718285339085,128.75)) ;
#12668=CARTESIAN_POINT('Origin',(0.,-25.,143.25)) ;
#12669=CARTESIAN_POINT('Origin',(0.,-25.,142.15)) ;
#12670=CARTESIAN_POINT('',(-0.719138307906,-23.6836261572,142.15)) ;
#12671=CARTESIAN_POINT('',(-0.719138307906306,-23.6836261571644,142.15)) ;
#12672=CARTESIAN_POINT('Origin',(0.,-25.,142.15)) ;
#12673=CARTESIAN_POINT('Origin',(0.,-25.,128.75)) ;
#12674=CARTESIAN_POINT('',(-0.719138307906,-23.6836261572,114.05)) ;
#12675=CARTESIAN_POINT('',(-0.719138307906306,-23.6836261571644,128.75)) ;
#12676=CARTESIAN_POINT('Origin',(0.,-25.,114.05)) ;
#12677=CARTESIAN_POINT('Origin',(0.,-25.,113.75)) ;
#12678=CARTESIAN_POINT('',(-0.575310646325,-23.9469009257,113.75)) ;
#12679=CARTESIAN_POINT('',(-0.575310646325044,-23.9469009257316,113.75)) ;
#12680=CARTESIAN_POINT('Origin',(0.,-25.,113.75)) ;
#12681=CARTESIAN_POINT('Origin',(0.,-26.2,113.75)) ;
#12682=CARTESIAN_POINT('Origin',(0.,-24.6,142.25)) ;
#12683=CARTESIAN_POINT('',(0.4,-24.6,142.25)) ;
#12684=CARTESIAN_POINT('',(-0.4,-24.6,142.25)) ;
#12685=CARTESIAN_POINT('',(-0.2,-24.6,142.25)) ;
#12686=CARTESIAN_POINT('',(0.4,-23.25,143.6)) ;
#12687=CARTESIAN_POINT('',(0.4,-23.925,142.925)) ;
#12688=CARTESIAN_POINT('',(-0.4,-23.25,143.6)) ;
#12689=CARTESIAN_POINT('',(5.55111512313E-17,-23.25,143.6)) ;
#12690=CARTESIAN_POINT('',(-0.4,-23.925,142.925)) ;
#12691=CARTESIAN_POINT('Origin',(0.,-25.4,142.25)) ;
#12692=CARTESIAN_POINT('',(0.4,-26.75,143.6)) ;
#12693=CARTESIAN_POINT('',(-0.4,-26.75,143.6)) ;
#12694=CARTESIAN_POINT('',(5.55111512313E-17,-26.75,143.6)) ;
#12695=CARTESIAN_POINT('',(0.4,-25.4,142.25)) ;
#12696=CARTESIAN_POINT('',(0.4,-26.075,142.925)) ;
#12697=CARTESIAN_POINT('',(-0.4,-25.4,142.25)) ;
#12698=CARTESIAN_POINT('',(0.2,-25.4,142.25)) ;
#12699=CARTESIAN_POINT('',(-0.4,-26.075,142.925)) ;
#12700=CARTESIAN_POINT('Origin',(0.,-23.25,143.6)) ;
#12701=CARTESIAN_POINT('',(0.4,-23.25,143.75)) ;
#12702=CARTESIAN_POINT('',(0.4,-23.25,143.675)) ;
#12703=CARTESIAN_POINT('',(-0.4,-23.25,143.75)) ;
#12704=CARTESIAN_POINT('',(5.55111512313E-17,-23.25,143.75)) ;
#12705=CARTESIAN_POINT('',(-0.4,-23.25,143.675)) ;
#12706=CARTESIAN_POINT('Origin',(0.,-26.75,143.6)) ;
#12707=CARTESIAN_POINT('',(0.4,-26.75,143.75)) ;
#12708=CARTESIAN_POINT('',(-0.4,-26.75,143.75)) ;
#12709=CARTESIAN_POINT('',(5.55111512313E-17,-26.75,143.75)) ;
#12710=CARTESIAN_POINT('',(0.4,-26.75,143.675)) ;
#12711=CARTESIAN_POINT('',(-0.4,-26.75,143.675)) ;
#12712=CARTESIAN_POINT('Origin',(-0.4,0.,0.)) ;
#12713=CARTESIAN_POINT('',(-0.4,-24.6,143.75)) ;
#12714=CARTESIAN_POINT('',(-0.4,-23.925,143.75)) ;
#12715=CARTESIAN_POINT('',(-0.4,-24.6,143.)) ;
#12716=CARTESIAN_POINT('Origin',(-0.4,0.,0.)) ;
#12717=CARTESIAN_POINT('',(-0.4,-25.4,143.75)) ;
#12718=CARTESIAN_POINT('',(-0.4,-26.075,143.75)) ;
#12719=CARTESIAN_POINT('',(-0.4,-25.4,143.)) ;
#12720=CARTESIAN_POINT('Origin',(0.4,0.,0.)) ;
#12721=CARTESIAN_POINT('',(0.4,-24.6,143.75)) ;
#12722=CARTESIAN_POINT('',(0.4,-24.6,143.)) ;
#12723=CARTESIAN_POINT('',(0.4,-23.925,143.75)) ;
#12724=CARTESIAN_POINT('Origin',(0.4,0.,0.)) ;
#12725=CARTESIAN_POINT('',(0.4,-25.4,143.75)) ;
#12726=CARTESIAN_POINT('',(0.4,-25.4,143.)) ;
#12727=CARTESIAN_POINT('',(0.4,-26.075,143.75)) ;
#12728=CARTESIAN_POINT('Origin',(0.,-25.,143.75)) ;
#12729=CARTESIAN_POINT('',(1.75,-24.6,143.75)) ;
#12730=CARTESIAN_POINT('',(1.075,-24.6,143.75)) ;
#12731=CARTESIAN_POINT('',(1.75,-25.4,143.75)) ;
#12732=CARTESIAN_POINT('',(1.75,-25.,143.75)) ;
#12733=CARTESIAN_POINT('',(1.075,-25.4,143.75)) ;
#12734=CARTESIAN_POINT('',(-1.75,-25.4,143.75)) ;
#12735=CARTESIAN_POINT('',(-1.075,-25.4,143.75)) ;
#12736=CARTESIAN_POINT('',(-1.75,-24.6,143.75)) ;
#12737=CARTESIAN_POINT('',(-1.75,-25.,143.75)) ;
#12738=CARTESIAN_POINT('',(-1.075,-24.6,143.75)) ;
#12739=CARTESIAN_POINT('Origin',(0.4,-25.,142.25)) ;
#12740=CARTESIAN_POINT('',(1.75,-24.6,143.6)) ;
#12741=CARTESIAN_POINT('',(1.75,-25.4,143.6)) ;
#12742=CARTESIAN_POINT('',(1.75,-25.,143.6)) ;
#12743=CARTESIAN_POINT('',(1.075,-24.6,142.925)) ;
#12744=CARTESIAN_POINT('',(0.4,-24.8,142.25)) ;
#12745=CARTESIAN_POINT('',(1.075,-25.4,142.925)) ;
#12746=CARTESIAN_POINT('Origin',(1.75,-25.,143.6)) ;
#12747=CARTESIAN_POINT('',(1.75,-24.6,143.675)) ;
#12748=CARTESIAN_POINT('',(1.75,-25.4,143.675)) ;
#12749=CARTESIAN_POINT('Origin',(-25.,-24.6,0.)) ;
#12750=CARTESIAN_POINT('Origin',(-25.,-25.4,0.)) ;
#12751=CARTESIAN_POINT('Origin',(-0.4,-25.,142.25)) ;
#12752=CARTESIAN_POINT('',(-0.4,-25.2,142.25)) ;
#12753=CARTESIAN_POINT('',(-1.75,-24.6,143.6)) ;
#12754=CARTESIAN_POINT('',(-1.075,-24.6,142.925)) ;
#12755=CARTESIAN_POINT('',(-1.75,-25.4,143.6)) ;
#12756=CARTESIAN_POINT('',(-1.75,-25.,143.6)) ;
#12757=CARTESIAN_POINT('',(-1.075,-25.4,142.925)) ;
#12758=CARTESIAN_POINT('Origin',(-25.,-24.6,0.)) ;
#12759=CARTESIAN_POINT('',(-1.75,-24.6,143.675)) ;
#12760=CARTESIAN_POINT('Origin',(-1.75,-25.,143.6)) ;
#12761=CARTESIAN_POINT('',(-1.75,-25.4,143.675)) ;
#12762=CARTESIAN_POINT('Origin',(-25.,-25.4,0.)) ;
#12763=CARTESIAN_POINT('Origin',(0.,-25.,142.25)) ;
#13484=UNCERTAINTY_MEASURE_WITH_UNIT(LENGTH_MEASURE(0.01),#13511,
'DISTANCE_ACCURACY_VALUE',
'Maximum model space distance between geometric entities at asserted c
onnectivities') ;
#13493=UNCERTAINTY_MEASURE_WITH_UNIT(LENGTH_MEASURE(0.01),#13511,
'DISTANCE_ACCURACY_VALUE',
'Maximum model space distance between geometric entities at asserted c
onnectivities') ;
#13501=(
GEOMETRIC_REPRESENTATION_CONTEXT(3)
GLOBAL_UNCERTAINTY_ASSIGNED_CONTEXT((#13484))
GLOBAL_UNIT_ASSIGNED_CONTEXT((#13511,#13513,#13514))
REPRESENTATION_CONTEXT('','3D')
) ;
#13510=(
GEOMETRIC_REPRESENTATION_CONTEXT(3)
GLOBAL_UNCERTAINTY_ASSIGNED_CONTEXT((#13493))
GLOBAL_UNIT_ASSIGNED_CONTEXT((#13511,#13513,#13514))
REPRESENTATION_CONTEXT('','3D')
) ;
#13511=(
LENGTH_UNIT()
NAMED_UNIT(*)
SI_UNIT(.MILLI.,.METRE.)
) ;
#13513=(
NAMED_UNIT(*)
PLANE_ANGLE_UNIT()
SI_UNIT($,.RADIAN.)
) ;
#13514=(
NAMED_UNIT(*)
SI_UNIT($,.STERADIAN.)
SOLID_ANGLE_UNIT()
) ;
#13522=SHAPE_DEFINITION_REPRESENTATION(#13538,#13569) ;
#13538=PRODUCT_DEFINITION_SHAPE('',$,#13586) ;
#13569=SHAPE_REPRESENTATION('',(#8165),#13501) ;
#13578=PRODUCT_DEFINITION_CONTEXT('part definition',#13628,'design') ;
#13586=PRODUCT_DEFINITION('Cover_Screw_1','Cover_Screw_1',#13602,#13578) ;
#13602=PRODUCT_DEFINITION_FORMATION('',$,#13637) ;
#13628=APPLICATION_CONTEXT(
'Core Data for Automotive Mechanical Design Process') ;
#13629=PRODUCT_CONTEXT('part definition',#13628,'mechanical') ;
#13637=PRODUCT('Cover_Screw_1','Cover_Screw_1',$,(#13629)) ;
#13650=PRESENTATION_STYLE_ASSIGNMENT((#13655)) ;
#13655=SURFACE_STYLE_USAGE(.BOTH.,#13660) ;
#13660=SURFACE_SIDE_STYLE('',(#13665)) ;
#13665=SURFACE_STYLE_FILL_AREA(#13670) ;
#13670=FILL_AREA_STYLE('Opaque(144,144,144)',(#13675)) ;
#13675=FILL_AREA_STYLE_COLOUR('Opaque(144,144,144)',#13680) ;
#13680=COLOUR_RGB('Opaque(144,144,144)', 0.40784314, 0.44705882, 0.49803922) ;
ENDSEC;
END-ISO-10303-21;
